ISO-10303-21;
HEADER;
/* Generated by software containing ST-Developer
 * from STEP Tools, Inc. (www.steptools.com) 
 */

FILE_DESCRIPTION(
/* description */ ('Bin tilter linkage'),
/* implementation_level */ '2;1');

FILE_NAME(
/* name */ 'Bearing cap (7).step',
/* time_stamp */ '2026-10-28T03:26:24-07:00',
/* author */ (''),
/* organization */ (''),
/* preprocessor_version */ 'ST-DEVELOPER v20.2',
/* originating_system */ 'Autodesk Translation Framework v15.17.0.0',
/* authorisation */ '');

FILE_SCHEMA (('AUTOMOTIVE_DESIGN { 1 0 10303 214 3 1 1 }'));
ENDSEC;

DATA;
#10=MECHANICAL_DESIGN_GEOMETRIC_PRESENTATION_REPRESENTATION('',(#929),#23728);
#717=SHAPE_REPRESENTATION_RELATIONSHIP('SRR','None',#24183,#823);
#823=ADVANCED_BREP_SHAPE_REPRESENTATION('',(#1042),#23683);
#929=STYLED_ITEM('',(#24765),#1042);
#1042=MANIFOLD_SOLID_BREP('Body1',#12460);
#1372=FACE_BOUND('',#3436,.T.);
#1373=FACE_BOUND('',#3437,.T.);
#1374=FACE_BOUND('',#3438,.T.);
#1375=FACE_BOUND('',#3439,.T.);
#1376=FACE_BOUND('',#3440,.T.);
#1377=FACE_BOUND('',#3442,.T.);
#1378=FACE_BOUND('',#3443,.T.);
#1379=FACE_BOUND('',#3444,.T.);
#1380=FACE_BOUND('',#3445,.T.);
#1381=FACE_BOUND('',#3446,.T.);
#1723=PLANE('',#14731);
#1724=PLANE('',#14732);
#2367=FACE_OUTER_BOUND('',#3429,.T.);
#2368=FACE_OUTER_BOUND('',#3430,.T.);
#2369=FACE_OUTER_BOUND('',#3431,.T.);
#2370=FACE_OUTER_BOUND('',#3432,.T.);
#2371=FACE_OUTER_BOUND('',#3433,.T.);
#2372=FACE_OUTER_BOUND('',#3434,.T.);
#2373=FACE_OUTER_BOUND('',#3435,.T.);
#2374=FACE_OUTER_BOUND('',#3441,.T.);
#3429=EDGE_LOOP('',(#10129,#10130,#10131,#10132));
#3430=EDGE_LOOP('',(#10133,#10134,#10135,#10136));
#3431=EDGE_LOOP('',(#10137,#10138,#10139,#10140));
#3432=EDGE_LOOP('',(#10141,#10142,#10143,#10144));
#3433=EDGE_LOOP('',(#10145,#10146,#10147,#10148));
#3434=EDGE_LOOP('',(#10149,#10150,#10151,#10152));
#3435=EDGE_LOOP('',(#10153));
#3436=EDGE_LOOP('',(#10154));
#3437=EDGE_LOOP('',(#10155));
#3438=EDGE_LOOP('',(#10156));
#3439=EDGE_LOOP('',(#10157));
#3440=EDGE_LOOP('',(#10158));
#3441=EDGE_LOOP('',(#10159));
#3442=EDGE_LOOP('',(#10160));
#3443=EDGE_LOOP('',(#10161));
#3444=EDGE_LOOP('',(#10162));
#3445=EDGE_LOOP('',(#10163));
#3446=EDGE_LOOP('',(#10164));
#4239=LINE('',#21760,#4914);
#4240=LINE('',#21766,#4915);
#4241=LINE('',#21772,#4916);
#4242=LINE('',#21778,#4917);
#4243=LINE('',#21784,#4918);
#4244=LINE('',#21790,#4919);
#4914=VECTOR('',#17942,0.225000000000001);
#4915=VECTOR('',#17949,0.225000000000001);
#4916=VECTOR('',#17956,0.225000000000001);
#4917=VECTOR('',#17963,0.225000000000001);
#4918=VECTOR('',#17970,1.02);
#4919=VECTOR('',#17977,2.2);
#5687=CIRCLE('',#14714,0.225000000000001);
#5688=CIRCLE('',#14715,0.225000000000001);
#5689=CIRCLE('',#14717,0.225000000000001);
#5690=CIRCLE('',#14718,0.225000000000001);
#5691=CIRCLE('',#14720,0.225000000000001);
#5692=CIRCLE('',#14721,0.225000000000001);
#5693=CIRCLE('',#14723,0.225000000000001);
#5694=CIRCLE('',#14724,0.225000000000001);
#5695=CIRCLE('',#14726,1.02);
#5696=CIRCLE('',#14727,1.02);
#5697=CIRCLE('',#14729,2.2);
#5698=CIRCLE('',#14730,2.2);
#6541=VERTEX_POINT('',#21757);
#6542=VERTEX_POINT('',#21759);
#6543=VERTEX_POINT('',#21763);
#6544=VERTEX_POINT('',#21765);
#6545=VERTEX_POINT('',#21769);
#6546=VERTEX_POINT('',#21771);
#6547=VERTEX_POINT('',#21775);
#6548=VERTEX_POINT('',#21777);
#6549=VERTEX_POINT('',#21781);
#6550=VERTEX_POINT('',#21783);
#6551=VERTEX_POINT('',#21787);
#6552=VERTEX_POINT('',#21789);
#7804=EDGE_CURVE('',#6541,#6541,#5687,.T.);
#7805=EDGE_CURVE('',#6541,#6542,#4239,.T.);
#7806=EDGE_CURVE('',#6542,#6542,#5688,.T.);
#7807=EDGE_CURVE('',#6543,#6543,#5689,.T.);
#7808=EDGE_CURVE('',#6543,#6544,#4240,.T.);
#7809=EDGE_CURVE('',#6544,#6544,#5690,.T.);
#7810=EDGE_CURVE('',#6545,#6545,#5691,.T.);
#7811=EDGE_CURVE('',#6545,#6546,#4241,.T.);
#7812=EDGE_CURVE('',#6546,#6546,#5692,.T.);
#7813=EDGE_CURVE('',#6547,#6547,#5693,.T.);
#7814=EDGE_CURVE('',#6547,#6548,#4242,.T.);
#7815=EDGE_CURVE('',#6548,#6548,#5694,.T.);
#7816=EDGE_CURVE('',#6549,#6549,#5695,.T.);
#7817=EDGE_CURVE('',#6549,#6550,#4243,.T.);
#7818=EDGE_CURVE('',#6550,#6550,#5696,.T.);
#7819=EDGE_CURVE('',#6551,#6551,#5697,.T.);
#7820=EDGE_CURVE('',#6551,#6552,#4244,.T.);
#7821=EDGE_CURVE('',#6552,#6552,#5698,.T.);
#10129=ORIENTED_EDGE('',*,*,#7804,.F.);
#10130=ORIENTED_EDGE('',*,*,#7805,.T.);
#10131=ORIENTED_EDGE('',*,*,#7806,.F.);
#10132=ORIENTED_EDGE('',*,*,#7805,.F.);
#10133=ORIENTED_EDGE('',*,*,#7807,.F.);
#10134=ORIENTED_EDGE('',*,*,#7808,.T.);
#10135=ORIENTED_EDGE('',*,*,#7809,.F.);
#10136=ORIENTED_EDGE('',*,*,#7808,.F.);
#10137=ORIENTED_EDGE('',*,*,#7810,.F.);
#10138=ORIENTED_EDGE('',*,*,#7811,.T.);
#10139=ORIENTED_EDGE('',*,*,#7812,.F.);
#10140=ORIENTED_EDGE('',*,*,#7811,.F.);
#10141=ORIENTED_EDGE('',*,*,#7813,.F.);
#10142=ORIENTED_EDGE('',*,*,#7814,.T.);
#10143=ORIENTED_EDGE('',*,*,#7815,.F.);
#10144=ORIENTED_EDGE('',*,*,#7814,.F.);
#10145=ORIENTED_EDGE('',*,*,#7816,.F.);
#10146=ORIENTED_EDGE('',*,*,#7817,.T.);
#10147=ORIENTED_EDGE('',*,*,#7818,.T.);
#10148=ORIENTED_EDGE('',*,*,#7817,.F.);
#10149=ORIENTED_EDGE('',*,*,#7819,.F.);
#10150=ORIENTED_EDGE('',*,*,#7820,.T.);
#10151=ORIENTED_EDGE('',*,*,#7821,.T.);
#10152=ORIENTED_EDGE('',*,*,#7820,.F.);
#10153=ORIENTED_EDGE('',*,*,#7819,.T.);
#10154=ORIENTED_EDGE('',*,*,#7816,.T.);
#10155=ORIENTED_EDGE('',*,*,#7815,.T.);
#10156=ORIENTED_EDGE('',*,*,#7812,.T.);
#10157=ORIENTED_EDGE('',*,*,#7809,.T.);
#10158=ORIENTED_EDGE('',*,*,#7806,.T.);
#10159=ORIENTED_EDGE('',*,*,#7821,.F.);
#10160=ORIENTED_EDGE('',*,*,#7818,.F.);
#10161=ORIENTED_EDGE('',*,*,#7813,.T.);
#10162=ORIENTED_EDGE('',*,*,#7810,.T.);
#10163=ORIENTED_EDGE('',*,*,#7807,.T.);
#10164=ORIENTED_EDGE('',*,*,#7804,.T.);
#11509=CYLINDRICAL_SURFACE('',#14713,0.225000000000001);
#11510=CYLINDRICAL_SURFACE('',#14716,0.225000000000001);
#11511=CYLINDRICAL_SURFACE('',#14719,0.225000000000001);
#11512=CYLINDRICAL_SURFACE('',#14722,0.225000000000001);
#11513=CYLINDRICAL_SURFACE('',#14725,1.02);
#11514=CYLINDRICAL_SURFACE('',#14728,2.2);
#12092=ADVANCED_FACE('',(#2367),#11509,.F.);
#12093=ADVANCED_FACE('',(#2368),#11510,.F.);
#12094=ADVANCED_FACE('',(#2369),#11511,.F.);
#12095=ADVANCED_FACE('',(#2370),#11512,.F.);
#12096=ADVANCED_FACE('',(#2371),#11513,.F.);
#12097=ADVANCED_FACE('',(#2372),#11514,.T.);
#12098=ADVANCED_FACE('',(#2373,#1372,#1373,#1374,#1375,#1376),#1723,.T.);
#12099=ADVANCED_FACE('',(#2374,#1377,#1378,#1379,#1380,#1381),#1724,.F.);
#12460=CLOSED_SHELL('',(#12092,#12093,#12094,#12095,#12096,#12097,#12098,
#12099));
#14712=AXIS2_PLACEMENT_3D('',#21755,#17936,#17937);
#14713=AXIS2_PLACEMENT_3D('',#21756,#17938,#17939);
#14714=AXIS2_PLACEMENT_3D('',#21758,#17940,#17941);
#14715=AXIS2_PLACEMENT_3D('',#21761,#17943,#17944);
#14716=AXIS2_PLACEMENT_3D('',#21762,#17945,#17946);
#14717=AXIS2_PLACEMENT_3D('',#21764,#17947,#17948);
#14718=AXIS2_PLACEMENT_3D('',#21767,#17950,#17951);
#14719=AXIS2_PLACEMENT_3D('',#21768,#17952,#17953);
#14720=AXIS2_PLACEMENT_3D('',#21770,#17954,#17955);
#14721=AXIS2_PLACEMENT_3D('',#21773,#17957,#17958);
#14722=AXIS2_PLACEMENT_3D('',#21774,#17959,#17960);
#14723=AXIS2_PLACEMENT_3D('',#21776,#17961,#17962);
#14724=AXIS2_PLACEMENT_3D('',#21779,#17964,#17965);
#14725=AXIS2_PLACEMENT_3D('',#21780,#17966,#17967);
#14726=AXIS2_PLACEMENT_3D('',#21782,#17968,#17969);
#14727=AXIS2_PLACEMENT_3D('',#21785,#17971,#17972);
#14728=AXIS2_PLACEMENT_3D('',#21786,#17973,#17974);
#14729=AXIS2_PLACEMENT_3D('',#21788,#17975,#17976);
#14730=AXIS2_PLACEMENT_3D('',#21791,#17978,#17979);
#14731=AXIS2_PLACEMENT_3D('',#21792,#17980,#17981);
#14732=AXIS2_PLACEMENT_3D('',#21793,#17982,#17983);
#17936=DIRECTION('axis',(0.,0.,1.));
#17937=DIRECTION('refdir',(1.,0.,0.));
#17938=DIRECTION('center_axis',(0.,1.,0.));
#17939=DIRECTION('ref_axis',(1.,0.,0.));
#17940=DIRECTION('center_axis',(0.,1.,0.));
#17941=DIRECTION('ref_axis',(1.,0.,0.));
#17942=DIRECTION('',(0.,1.,0.));
#17943=DIRECTION('center_axis',(0.,-1.,0.));
#17944=DIRECTION('ref_axis',(1.,0.,0.));
#17945=DIRECTION('center_axis',(0.,1.,0.));
#17946=DIRECTION('ref_axis',(1.,0.,0.));
#17947=DIRECTION('center_axis',(0.,1.,0.));
#17948=DIRECTION('ref_axis',(1.,0.,0.));
#17949=DIRECTION('',(0.,1.,0.));
#17950=DIRECTION('center_axis',(0.,-1.,0.));
#17951=DIRECTION('ref_axis',(1.,0.,0.));
#17952=DIRECTION('center_axis',(0.,1.,0.));
#17953=DIRECTION('ref_axis',(1.,0.,0.));
#17954=DIRECTION('center_axis',(0.,1.,0.));
#17955=DIRECTION('ref_axis',(1.,0.,0.));
#17956=DIRECTION('',(0.,1.,0.));
#17957=DIRECTION('center_axis',(0.,-1.,0.));
#17958=DIRECTION('ref_axis',(1.,0.,0.));
#17959=DIRECTION('center_axis',(0.,1.,0.));
#17960=DIRECTION('ref_axis',(1.,0.,0.));
#17961=DIRECTION('center_axis',(0.,1.,0.));
#17962=DIRECTION('ref_axis',(1.,0.,0.));
#17963=DIRECTION('',(0.,1.,0.));
#17964=DIRECTION('center_axis',(0.,-1.,0.));
#17965=DIRECTION('ref_axis',(1.,0.,0.));
#17966=DIRECTION('center_axis',(0.,1.,0.));
#17967=DIRECTION('ref_axis',(1.,0.,0.));
#17968=DIRECTION('center_axis',(0.,-1.,0.));
#17969=DIRECTION('ref_axis',(1.,0.,0.));
#17970=DIRECTION('',(0.,-1.,0.));
#17971=DIRECTION('center_axis',(0.,-1.,0.));
#17972=DIRECTION('ref_axis',(1.,0.,0.));
#17973=DIRECTION('center_axis',(0.,1.,0.));
#17974=DIRECTION('ref_axis',(1.,0.,0.));
#17975=DIRECTION('center_axis',(0.,1.,0.));
#17976=DIRECTION('ref_axis',(1.,0.,0.));
#17977=DIRECTION('',(0.,-1.,0.));
#17978=DIRECTION('center_axis',(0.,1.,0.));
#17979=DIRECTION('ref_axis',(1.,0.,0.));
#17980=DIRECTION('center_axis',(0.,1.,0.));
#17981=DIRECTION('ref_axis',(1.,0.,0.));
#17982=DIRECTION('center_axis',(0.,1.,0.));
#17983=DIRECTION('ref_axis',(1.,0.,0.));
#21755=CARTESIAN_POINT('',(0.,0.,0.));
#21756=CARTESIAN_POINT('Origin',(22.893930933827,0.4,27.3496056572921));
#21757=CARTESIAN_POINT('',(22.668930933827,0.5,27.3496056572921));
#21758=CARTESIAN_POINT('Origin',(22.893930933827,0.5,27.3496056572921));
#21759=CARTESIAN_POINT('',(22.668930933827,0.8,27.3496056572921));
#21760=CARTESIAN_POINT('',(22.668930933827,0.4,27.3496056572921));
#21761=CARTESIAN_POINT('Origin',(22.893930933827,0.8,27.3496056572921));
#21762=CARTESIAN_POINT('Origin',(22.893930933827,0.4,29.9659007476824));
#21763=CARTESIAN_POINT('',(22.668930933827,0.5,29.9659007476824));
#21764=CARTESIAN_POINT('Origin',(22.893930933827,0.5,29.9659007476824));
#21765=CARTESIAN_POINT('',(22.668930933827,0.8,29.9659007476824));
#21766=CARTESIAN_POINT('',(22.668930933827,0.4,29.9659007476824));
#21767=CARTESIAN_POINT('Origin',(22.893930933827,0.8,29.9659007476824));
#21768=CARTESIAN_POINT('Origin',(25.5102260242172,0.4,29.9659007476824));
#21769=CARTESIAN_POINT('',(25.2852260242172,0.5,29.9659007476824));
#21770=CARTESIAN_POINT('Origin',(25.5102260242172,0.5,29.9659007476824));
#21771=CARTESIAN_POINT('',(25.2852260242172,0.8,29.9659007476824));
#21772=CARTESIAN_POINT('',(25.2852260242172,0.4,29.9659007476824));
#21773=CARTESIAN_POINT('Origin',(25.5102260242172,0.8,29.9659007476824));
#21774=CARTESIAN_POINT('Origin',(25.5102260242172,0.4,27.3496056572921));
#21775=CARTESIAN_POINT('',(25.2852260242172,0.5,27.3496056572921));
#21776=CARTESIAN_POINT('Origin',(25.5102260242172,0.5,27.3496056572921));
#21777=CARTESIAN_POINT('',(25.2852260242172,0.8,27.3496056572921));
#21778=CARTESIAN_POINT('',(25.2852260242172,0.4,27.3496056572921));
#21779=CARTESIAN_POINT('Origin',(25.5102260242172,0.8,27.3496056572921));
#21780=CARTESIAN_POINT('Origin',(24.2020784790221,0.5,28.6577532024872));
#21781=CARTESIAN_POINT('',(23.1820784790221,0.8,28.6577532024872));
#21782=CARTESIAN_POINT('Origin',(24.2020784790221,0.8,28.6577532024872));
#21783=CARTESIAN_POINT('',(23.1820784790221,0.5,28.6577532024872));
#21784=CARTESIAN_POINT('',(23.1820784790221,0.5,28.6577532024872));
#21785=CARTESIAN_POINT('Origin',(24.2020784790221,0.5,28.6577532024872));
#21786=CARTESIAN_POINT('Origin',(24.2020784790221,0.5,28.6577532024872));
#21787=CARTESIAN_POINT('',(22.0020784790221,0.8,28.6577532024872));
#21788=CARTESIAN_POINT('Origin',(24.2020784790221,0.8,28.6577532024872));
#21789=CARTESIAN_POINT('',(22.0020784790221,0.5,28.6577532024872));
#21790=CARTESIAN_POINT('',(22.0020784790221,0.5,28.6577532024872));
#21791=CARTESIAN_POINT('Origin',(24.2020784790221,0.5,28.6577532024872));
#21792=CARTESIAN_POINT('Origin',(24.2020784790221,0.8,28.6577532024872));
#21793=CARTESIAN_POINT('Origin',(24.2020784790221,0.5,28.6577532024872));
#23566=UNCERTAINTY_MEASURE_WITH_UNIT(LENGTH_MEASURE(0.001),#23729,
'DISTANCE_ACCURACY_VALUE',
'Maximum model space distance between geometric entities at asserted c
onnectivities');
#23611=UNCERTAINTY_MEASURE_WITH_UNIT(LENGTH_MEASURE(0.001),#23729,
'DISTANCE_ACCURACY_VALUE',
'Maximum model space distance between geometric entities at asserted c
onnectivities');
#23683=(
GEOMETRIC_REPRESENTATION_CONTEXT(3)
GLOBAL_UNCERTAINTY_ASSIGNED_CONTEXT((#23566))
GLOBAL_UNIT_ASSIGNED_CONTEXT((#23729,#23731,#23732))
REPRESENTATION_CONTEXT('','3D')
);
#23728=(
GEOMETRIC_REPRESENTATION_CONTEXT(3)
GLOBAL_UNCERTAINTY_ASSIGNED_CONTEXT((#23611))
GLOBAL_UNIT_ASSIGNED_CONTEXT((#23729,#23731,#23732))
REPRESENTATION_CONTEXT('','3D')
);
#23729=(
LENGTH_UNIT()
NAMED_UNIT(*)
SI_UNIT(.CENTI.,.METRE.)
);
#23731=(
NAMED_UNIT(*)
PLANE_ANGLE_UNIT()
SI_UNIT($,.RADIAN.)
);
#23732=(
NAMED_UNIT(*)
SI_UNIT($,.STERADIAN.)
SOLID_ANGLE_UNIT()
);
#23804=SHAPE_DEFINITION_REPRESENTATION(#23920,#24183);
#23920=PRODUCT_DEFINITION_SHAPE('',$,#24300);
#24183=SHAPE_REPRESENTATION('',(#14712),#23683);
#24228=PRODUCT_DEFINITION_CONTEXT('part definition',#24578,'design');
#24300=PRODUCT_DEFINITION('Bearing cap (7)','Bearing cap (7)',#24416,#24228);
#24416=PRODUCT_DEFINITION_FORMATION('',$,#24651);
#24578=APPLICATION_CONTEXT(
'Core Data for Automotive Mechanical Design Process');
#24579=PRODUCT_CONTEXT('part definition',#24578,'mechanical');
#24651=PRODUCT('Bearing cap (7)','Bearing cap (7)','Bearing cap (7)',(#24579));
#24759=COLOUR_RGB('Grey',0.48,0.52,0.57);
#24760=FILL_AREA_STYLE_COLOUR('',#24759);
#24761=FILL_AREA_STYLE('',(#24760));
#24762=SURFACE_STYLE_FILL_AREA(#24761);
#24763=SURFACE_SIDE_STYLE('',(#24762));
#24764=SURFACE_STYLE_USAGE(.BOTH.,#24763);
#24765=PRESENTATION_STYLE_ASSIGNMENT((#24764));
ENDSEC;
END-ISO-10303-21;
